ISO-10303-21;
HEADER;
/* Generated by software containing ST-Developer
 * from STEP Tools, Inc. (www.steptools.com) 
 */

FILE_DESCRIPTION(
/* description */ ('Guided pneumatic stop gate'),
/* implementation_level */ '2;1');

FILE_NAME(
/* name */ 'Hex Nut - M5.step',
/* time_stamp */ '2026-10-27T21:43:45-07:00',
/* author */ (''),
/* organization */ (''),
/* preprocessor_version */ 'ST-DEVELOPER v20.2',
/* originating_system */ 'Autodesk Translation Framework v15.17.0.0',
/* authorisation */ '');

FILE_SCHEMA (('AUTOMOTIVE_DESIGN { 1 0 10303 214 3 1 1 }'));
ENDSEC;

DATA;
#10=MECHANICAL_DESIGN_GEOMETRIC_PRESENTATION_REPRESENTATION('',(#553),#14392);
#19=(
BOUNDED_CURVE()
B_SPLINE_CURVE(2,(#12867,#12868,#12869),.UNSPECIFIED.,.F.,.F.)
B_SPLINE_CURVE_WITH_KNOTS((3,3),(0.140651836354967,0.670383167684795),
 .UNSPECIFIED.)
CURVE()
GEOMETRIC_REPRESENTATION_ITEM()
RATIONAL_B_SPLINE_CURVE((1.11602540378444,1.28867513459481,1.11602540378444))
REPRESENTATION_ITEM('')
);
#20=(
BOUNDED_CURVE()
B_SPLINE_CURVE(2,(#12871,#12872,#12873),.UNSPECIFIED.,.F.,.F.)
B_SPLINE_CURVE_WITH_KNOTS((3,3),(0.140651836354967,0.670383167684795),
 .UNSPECIFIED.)
CURVE()
GEOMETRIC_REPRESENTATION_ITEM()
RATIONAL_B_SPLINE_CURVE((1.11602540378444,1.28867513459481,1.11602540378444))
REPRESENTATION_ITEM('')
);
#21=(
BOUNDED_CURVE()
B_SPLINE_CURVE(2,(#12878,#12879,#12880),.UNSPECIFIED.,.F.,.F.)
B_SPLINE_CURVE_WITH_KNOTS((3,3),(0.140651836354967,0.670383167684795),
 .UNSPECIFIED.)
CURVE()
GEOMETRIC_REPRESENTATION_ITEM()
RATIONAL_B_SPLINE_CURVE((1.11602540378444,1.28867513459481,1.11602540378444))
REPRESENTATION_ITEM('')
);
#22=(
BOUNDED_CURVE()
B_SPLINE_CURVE(2,(#12882,#12883,#12884),.UNSPECIFIED.,.F.,.F.)
B_SPLINE_CURVE_WITH_KNOTS((3,3),(0.140651836354967,0.670383167684795),
 .UNSPECIFIED.)
CURVE()
GEOMETRIC_REPRESENTATION_ITEM()
RATIONAL_B_SPLINE_CURVE((1.11602540378444,1.28867513459481,1.11602540378444))
REPRESENTATION_ITEM('')
);
#23=(
BOUNDED_CURVE()
B_SPLINE_CURVE(2,(#12886,#12887,#12888),.UNSPECIFIED.,.F.,.F.)
B_SPLINE_CURVE_WITH_KNOTS((3,3),(0.140651836354967,0.670383167684795),
 .UNSPECIFIED.)
CURVE()
GEOMETRIC_REPRESENTATION_ITEM()
RATIONAL_B_SPLINE_CURVE((1.11602540378444,1.28867513459481,1.11602540378444))
REPRESENTATION_ITEM('')
);
#24=(
BOUNDED_CURVE()
B_SPLINE_CURVE(2,(#12889,#12890,#12891),.UNSPECIFIED.,.F.,.F.)
B_SPLINE_CURVE_WITH_KNOTS((3,3),(0.140651836354967,0.670383167684795),
 .UNSPECIFIED.)
CURVE()
GEOMETRIC_REPRESENTATION_ITEM()
RATIONAL_B_SPLINE_CURVE((1.11602540378444,1.28867513459481,1.11602540378444))
REPRESENTATION_ITEM('')
);
#25=(
BOUNDED_CURVE()
B_SPLINE_CURVE(2,(#12898,#12899,#12900),.UNSPECIFIED.,.F.,.F.)
B_SPLINE_CURVE_WITH_KNOTS((3,3),(0.140651836354967,0.670383167684795),
 .UNSPECIFIED.)
CURVE()
GEOMETRIC_REPRESENTATION_ITEM()
RATIONAL_B_SPLINE_CURVE((1.11602540378444,1.28867513459481,1.11602540378444))
REPRESENTATION_ITEM('')
);
#26=(
BOUNDED_CURVE()
B_SPLINE_CURVE(2,(#12902,#12903,#12904),.UNSPECIFIED.,.F.,.F.)
B_SPLINE_CURVE_WITH_KNOTS((3,3),(0.140651836354967,0.670383167684796),
 .UNSPECIFIED.)
CURVE()
GEOMETRIC_REPRESENTATION_ITEM()
RATIONAL_B_SPLINE_CURVE((1.11602540378444,1.28867513459481,1.11602540378444))
REPRESENTATION_ITEM('')
);
#27=(
BOUNDED_CURVE()
B_SPLINE_CURVE(2,(#12906,#12907,#12908),.UNSPECIFIED.,.F.,.F.)
B_SPLINE_CURVE_WITH_KNOTS((3,3),(0.140651836354967,0.670383167684795),
 .UNSPECIFIED.)
CURVE()
GEOMETRIC_REPRESENTATION_ITEM()
RATIONAL_B_SPLINE_CURVE((1.11602540378444,1.28867513459481,1.11602540378444))
REPRESENTATION_ITEM('')
);
#28=(
BOUNDED_CURVE()
B_SPLINE_CURVE(2,(#12910,#12911,#12912),.UNSPECIFIED.,.F.,.F.)
B_SPLINE_CURVE_WITH_KNOTS((3,3),(0.140651836354967,0.670383167684795),
 .UNSPECIFIED.)
CURVE()
GEOMETRIC_REPRESENTATION_ITEM()
RATIONAL_B_SPLINE_CURVE((1.11602540378444,1.28867513459482,1.11602540378444))
REPRESENTATION_ITEM('')
);
#29=(
BOUNDED_CURVE()
B_SPLINE_CURVE(2,(#12914,#12915,#12916),.UNSPECIFIED.,.F.,.F.)
B_SPLINE_CURVE_WITH_KNOTS((3,3),(0.140651836354967,0.670383167684795),
 .UNSPECIFIED.)
CURVE()
GEOMETRIC_REPRESENTATION_ITEM()
RATIONAL_B_SPLINE_CURVE((1.11602540378444,1.28867513459481,1.11602540378444))
REPRESENTATION_ITEM('')
);
#30=(
BOUNDED_CURVE()
B_SPLINE_CURVE(2,(#12917,#12918,#12919),.UNSPECIFIED.,.F.,.F.)
B_SPLINE_CURVE_WITH_KNOTS((3,3),(0.140651836354967,0.670383167684795),
 .UNSPECIFIED.)
CURVE()
GEOMETRIC_REPRESENTATION_ITEM()
RATIONAL_B_SPLINE_CURVE((1.11602540378444,1.28867513459481,1.11602540378444))
REPRESENTATION_ITEM('')
);
#432=CONICAL_SURFACE('',#8810,0.47094010767585,1.0471975511966);
#433=CONICAL_SURFACE('',#8812,0.47094010767585,1.0471975511966);
#469=SHAPE_REPRESENTATION_RELATIONSHIP('SRR','None',#14604,#511);
#511=ADVANCED_BREP_SHAPE_REPRESENTATION('',(#594),#14366);
#553=STYLED_ITEM('',(#14898),#594);
#594=MANIFOLD_SOLID_BREP('Body1',#7894);
#697=FACE_BOUND('',#1906,.T.);
#698=FACE_BOUND('',#1908,.T.);
#971=PLANE('',#8814);
#972=PLANE('',#8815);
#973=PLANE('',#8816);
#974=PLANE('',#8820);
#975=PLANE('',#8821);
#976=PLANE('',#8822);
#977=PLANE('',#8823);
#978=PLANE('',#8824);
#1339=FACE_OUTER_BOUND('',#1896,.T.);
#1340=FACE_OUTER_BOUND('',#1897,.T.);
#1341=FACE_OUTER_BOUND('',#1898,.T.);
#1342=FACE_OUTER_BOUND('',#1899,.T.);
#1343=FACE_OUTER_BOUND('',#1900,.T.);
#1344=FACE_OUTER_BOUND('',#1901,.T.);
#1345=FACE_OUTER_BOUND('',#1902,.T.);
#1346=FACE_OUTER_BOUND('',#1903,.T.);
#1347=FACE_OUTER_BOUND('',#1904,.T.);
#1348=FACE_OUTER_BOUND('',#1905,.T.);
#1349=FACE_OUTER_BOUND('',#1907,.T.);
#1896=EDGE_LOOP('',(#6172,#6173,#6174,#6175,#6176,#6177,#6178,#6179,#6180));
#1897=EDGE_LOOP('',(#6181,#6182,#6183,#6184,#6185,#6186,#6187,#6188,#6189));
#1898=EDGE_LOOP('',(#6190,#6191,#6192,#6193));
#1899=EDGE_LOOP('',(#6194,#6195,#6196,#6197));
#1900=EDGE_LOOP('',(#6198,#6199,#6200,#6201));
#1901=EDGE_LOOP('',(#6202,#6203,#6204,#6205));
#1902=EDGE_LOOP('',(#6206,#6207,#6208,#6209));
#1903=EDGE_LOOP('',(#6210,#6211,#6212,#6213));
#1904=EDGE_LOOP('',(#6214,#6215,#6216,#6217));
#1905=EDGE_LOOP('',(#6218));
#1906=EDGE_LOOP('',(#6219));
#1907=EDGE_LOOP('',(#6220));
#1908=EDGE_LOOP('',(#6221));
#2525=LINE('',#12875,#3070);
#2526=LINE('',#12896,#3071);
#2527=LINE('',#12921,#3072);
#2528=LINE('',#12922,#3073);
#2529=LINE('',#12924,#3074);
#2530=LINE('',#12926,#3075);
#2531=LINE('',#12931,#3076);
#2532=LINE('',#12934,#3077);
#2533=LINE('',#12936,#3078);
#3070=VECTOR('',#10482,0.47094010767585);
#3071=VECTOR('',#10489,0.47094010767585);
#3072=VECTOR('',#10492,1.);
#3073=VECTOR('',#10493,1.);
#3074=VECTOR('',#10496,1.);
#3075=VECTOR('',#10499,1.);
#3076=VECTOR('',#10504,0.25);
#3077=VECTOR('',#10509,1.);
#3078=VECTOR('',#10512,1.);
#3535=CIRCLE('',#8811,0.38);
#3536=CIRCLE('',#8813,0.38);
#3537=CIRCLE('',#8818,0.2117);
#3538=CIRCLE('',#8819,0.2117);
#4008=VERTEX_POINT('',#12865);
#4009=VERTEX_POINT('',#12866);
#4010=VERTEX_POINT('',#12870);
#4011=VERTEX_POINT('',#12874);
#4012=VERTEX_POINT('',#12877);
#4013=VERTEX_POINT('',#12881);
#4014=VERTEX_POINT('',#12885);
#4015=VERTEX_POINT('',#12893);
#4016=VERTEX_POINT('',#12895);
#4017=VERTEX_POINT('',#12897);
#4018=VERTEX_POINT('',#12901);
#4019=VERTEX_POINT('',#12905);
#4020=VERTEX_POINT('',#12909);
#4021=VERTEX_POINT('',#12913);
#4022=VERTEX_POINT('',#12928);
#4023=VERTEX_POINT('',#12930);
#4784=EDGE_CURVE('',#4008,#4009,#19,.T.);
#4785=EDGE_CURVE('',#4010,#4008,#20,.T.);
#4786=EDGE_CURVE('',#4010,#4011,#2525,.T.);
#4787=EDGE_CURVE('',#4011,#4011,#3535,.T.);
#4788=EDGE_CURVE('',#4012,#4010,#21,.T.);
#4789=EDGE_CURVE('',#4013,#4012,#22,.T.);
#4790=EDGE_CURVE('',#4014,#4013,#23,.T.);
#4791=EDGE_CURVE('',#4009,#4014,#24,.T.);
#4792=EDGE_CURVE('',#4015,#4015,#3536,.T.);
#4793=EDGE_CURVE('',#4015,#4016,#2526,.T.);
#4794=EDGE_CURVE('',#4017,#4016,#25,.T.);
#4795=EDGE_CURVE('',#4018,#4017,#26,.T.);
#4796=EDGE_CURVE('',#4019,#4018,#27,.T.);
#4797=EDGE_CURVE('',#4020,#4019,#28,.T.);
#4798=EDGE_CURVE('',#4021,#4020,#29,.T.);
#4799=EDGE_CURVE('',#4016,#4021,#30,.T.);
#4800=EDGE_CURVE('',#4012,#4021,#2527,.T.);
#4801=EDGE_CURVE('',#4013,#4020,#2528,.T.);
#4802=EDGE_CURVE('',#4010,#4016,#2529,.T.);
#4803=EDGE_CURVE('',#4008,#4017,#2530,.T.);
#4804=EDGE_CURVE('',#4022,#4022,#3537,.F.);
#4805=EDGE_CURVE('',#4022,#4023,#2531,.T.);
#4806=EDGE_CURVE('',#4023,#4023,#3538,.F.);
#4807=EDGE_CURVE('',#4009,#4018,#2532,.T.);
#4808=EDGE_CURVE('',#4014,#4019,#2533,.T.);
#6172=ORIENTED_EDGE('',*,*,#4784,.F.);
#6173=ORIENTED_EDGE('',*,*,#4785,.F.);
#6174=ORIENTED_EDGE('',*,*,#4786,.T.);
#6175=ORIENTED_EDGE('',*,*,#4787,.F.);
#6176=ORIENTED_EDGE('',*,*,#4786,.F.);
#6177=ORIENTED_EDGE('',*,*,#4788,.F.);
#6178=ORIENTED_EDGE('',*,*,#4789,.F.);
#6179=ORIENTED_EDGE('',*,*,#4790,.F.);
#6180=ORIENTED_EDGE('',*,*,#4791,.F.);
#6181=ORIENTED_EDGE('',*,*,#4792,.F.);
#6182=ORIENTED_EDGE('',*,*,#4793,.T.);
#6183=ORIENTED_EDGE('',*,*,#4794,.F.);
#6184=ORIENTED_EDGE('',*,*,#4795,.F.);
#6185=ORIENTED_EDGE('',*,*,#4796,.F.);
#6186=ORIENTED_EDGE('',*,*,#4797,.F.);
#6187=ORIENTED_EDGE('',*,*,#4798,.F.);
#6188=ORIENTED_EDGE('',*,*,#4799,.F.);
#6189=ORIENTED_EDGE('',*,*,#4793,.F.);
#6190=ORIENTED_EDGE('',*,*,#4789,.T.);
#6191=ORIENTED_EDGE('',*,*,#4800,.T.);
#6192=ORIENTED_EDGE('',*,*,#4798,.T.);
#6193=ORIENTED_EDGE('',*,*,#4801,.F.);
#6194=ORIENTED_EDGE('',*,*,#4788,.T.);
#6195=ORIENTED_EDGE('',*,*,#4802,.T.);
#6196=ORIENTED_EDGE('',*,*,#4799,.T.);
#6197=ORIENTED_EDGE('',*,*,#4800,.F.);
#6198=ORIENTED_EDGE('',*,*,#4785,.T.);
#6199=ORIENTED_EDGE('',*,*,#4803,.T.);
#6200=ORIENTED_EDGE('',*,*,#4794,.T.);
#6201=ORIENTED_EDGE('',*,*,#4802,.F.);
#6202=ORIENTED_EDGE('',*,*,#4804,.F.);
#6203=ORIENTED_EDGE('',*,*,#4805,.T.);
#6204=ORIENTED_EDGE('',*,*,#4806,.T.);
#6205=ORIENTED_EDGE('',*,*,#4805,.F.);
#6206=ORIENTED_EDGE('',*,*,#4784,.T.);
#6207=ORIENTED_EDGE('',*,*,#4807,.T.);
#6208=ORIENTED_EDGE('',*,*,#4795,.T.);
#6209=ORIENTED_EDGE('',*,*,#4803,.F.);
#6210=ORIENTED_EDGE('',*,*,#4790,.T.);
#6211=ORIENTED_EDGE('',*,*,#4801,.T.);
#6212=ORIENTED_EDGE('',*,*,#4797,.T.);
#6213=ORIENTED_EDGE('',*,*,#4808,.F.);
#6214=ORIENTED_EDGE('',*,*,#4791,.T.);
#6215=ORIENTED_EDGE('',*,*,#4808,.T.);
#6216=ORIENTED_EDGE('',*,*,#4796,.T.);
#6217=ORIENTED_EDGE('',*,*,#4807,.F.);
#6218=ORIENTED_EDGE('',*,*,#4792,.T.);
#6219=ORIENTED_EDGE('',*,*,#4804,.T.);
#6220=ORIENTED_EDGE('',*,*,#4787,.T.);
#6221=ORIENTED_EDGE('',*,*,#4806,.F.);
#7314=CYLINDRICAL_SURFACE('',#8817,0.2117);
#7621=ADVANCED_FACE('',(#1339),#432,.T.);
#7622=ADVANCED_FACE('',(#1340),#433,.T.);
#7623=ADVANCED_FACE('',(#1341),#971,.T.);
#7624=ADVANCED_FACE('',(#1342),#972,.T.);
#7625=ADVANCED_FACE('',(#1343),#973,.T.);
#7626=ADVANCED_FACE('',(#1344),#7314,.F.);
#7627=ADVANCED_FACE('',(#1345),#974,.T.);
#7628=ADVANCED_FACE('',(#1346),#975,.T.);
#7629=ADVANCED_FACE('',(#1347),#976,.T.);
#7630=ADVANCED_FACE('',(#1348,#697),#977,.T.);
#7631=ADVANCED_FACE('',(#1349,#698),#978,.F.);
#7894=CLOSED_SHELL('',(#7621,#7622,#7623,#7624,#7625,#7626,#7627,#7628,
#7629,#7630,#7631));
#8809=AXIS2_PLACEMENT_3D('',#12863,#10478,#10479);
#8810=AXIS2_PLACEMENT_3D('',#12864,#10480,#10481);
#8811=AXIS2_PLACEMENT_3D('',#12876,#10483,#10484);
#8812=AXIS2_PLACEMENT_3D('',#12892,#10485,#10486);
#8813=AXIS2_PLACEMENT_3D('',#12894,#10487,#10488);
#8814=AXIS2_PLACEMENT_3D('',#12920,#10490,#10491);
#8815=AXIS2_PLACEMENT_3D('',#12923,#10494,#10495);
#8816=AXIS2_PLACEMENT_3D('',#12925,#10497,#10498);
#8817=AXIS2_PLACEMENT_3D('',#12927,#10500,#10501);
#8818=AXIS2_PLACEMENT_3D('',#12929,#10502,#10503);
#8819=AXIS2_PLACEMENT_3D('',#12932,#10505,#10506);
#8820=AXIS2_PLACEMENT_3D('',#12933,#10507,#10508);
#8821=AXIS2_PLACEMENT_3D('',#12935,#10510,#10511);
#8822=AXIS2_PLACEMENT_3D('',#12937,#10513,#10514);
#8823=AXIS2_PLACEMENT_3D('',#12938,#10515,#10516);
#8824=AXIS2_PLACEMENT_3D('',#12939,#10517,#10518);
#10478=DIRECTION('axis',(0.,0.,1.));
#10479=DIRECTION('refdir',(1.,0.,0.));
#10480=DIRECTION('center_axis',(0.,1.,0.));
#10481=DIRECTION('ref_axis',(1.,0.,0.));
#10482=DIRECTION('',(0.866025403784439,-0.5,1.06057523872491E-16));
#10483=DIRECTION('center_axis',(0.,-1.,0.));
#10484=DIRECTION('ref_axis',(1.,0.,0.));
#10485=DIRECTION('center_axis',(0.,-1.,0.));
#10486=DIRECTION('ref_axis',(1.,0.,0.));
#10487=DIRECTION('center_axis',(0.,1.,0.));
#10488=DIRECTION('ref_axis',(1.,0.,0.));
#10489=DIRECTION('',(-0.866025403784439,-0.5,-1.06057523872491E-16));
#10490=DIRECTION('center_axis',(1.20185167898973E-16,0.,-1.));
#10491=DIRECTION('ref_axis',(-1.,0.,-1.20185167898973E-16));
#10492=DIRECTION('',(0.,1.,0.));
#10493=DIRECTION('',(0.,1.,0.));
#10494=DIRECTION('center_axis',(-0.866025403784439,0.,-0.5));
#10495=DIRECTION('ref_axis',(-0.5,0.,0.866025403784439));
#10496=DIRECTION('',(0.,1.,0.));
#10497=DIRECTION('center_axis',(-0.866025403784439,0.,0.5));
#10498=DIRECTION('ref_axis',(0.5,0.,0.866025403784439));
#10499=DIRECTION('',(0.,1.,0.));
#10500=DIRECTION('center_axis',(0.,1.,0.));
#10501=DIRECTION('ref_axis',(1.,0.,0.));
#10502=DIRECTION('center_axis',(0.,1.,0.));
#10503=DIRECTION('ref_axis',(1.,0.,0.));
#10504=DIRECTION('',(0.,-1.,0.));
#10505=DIRECTION('center_axis',(0.,1.,0.));
#10506=DIRECTION('ref_axis',(1.,0.,0.));
#10507=DIRECTION('center_axis',(-2.40370335797945E-16,0.,1.));
#10508=DIRECTION('ref_axis',(1.,0.,2.40370335797945E-16));
#10509=DIRECTION('',(0.,1.,0.));
#10510=DIRECTION('center_axis',(0.866025403784439,0.,-0.5));
#10511=DIRECTION('ref_axis',(-0.5,0.,-0.866025403784439));
#10512=DIRECTION('',(0.,1.,0.));
#10513=DIRECTION('center_axis',(0.866025403784439,0.,0.5));
#10514=DIRECTION('ref_axis',(0.5,0.,-0.866025403784439));
#10515=DIRECTION('center_axis',(0.,1.,0.));
#10516=DIRECTION('ref_axis',(1.,0.,0.));
#10517=DIRECTION('center_axis',(0.,1.,0.));
#10518=DIRECTION('ref_axis',(1.,0.,0.));
#12863=CARTESIAN_POINT('',(0.,0.,0.));
#12864=CARTESIAN_POINT('Origin',(0.,0.0525042956467857,0.));
#12865=CARTESIAN_POINT('',(-0.230940107675851,0.0472735643746089,0.4));
#12866=CARTESIAN_POINT('',(0.23094010767585,0.0472735643746089,0.4));
#12867=CARTESIAN_POINT('Ctrl Pts',(-0.230940107675851,0.0472735643746089,
0.4));
#12868=CARTESIAN_POINT('Ctrl Pts',(1.11022302462516E-16,-0.0193931022920578,
0.4));
#12869=CARTESIAN_POINT('Ctrl Pts',(0.23094010767585,0.0472735643746089,
0.4));
#12870=CARTESIAN_POINT('',(-0.461880215351701,0.0472735643746089,-5.6564012731995E-17));
#12871=CARTESIAN_POINT('Ctrl Pts',(-0.461880215351701,0.0472735643746089,
-5.6564012731995E-17));
#12872=CARTESIAN_POINT('Ctrl Pts',(-0.346410161513776,-0.0193931022920579,
0.2));
#12873=CARTESIAN_POINT('Ctrl Pts',(-0.230940107675851,0.0472735643746089,
0.4));
#12874=CARTESIAN_POINT('',(-0.38,-2.08166817117217E-17,-4.65365783675994E-17));
#12875=CARTESIAN_POINT('',(-0.47094010767585,0.0525042956467857,-5.7673529545534E-17));
#12876=CARTESIAN_POINT('Origin',(0.,0.,0.));
#12877=CARTESIAN_POINT('',(-0.23094010767585,0.0472735643746089,-0.4));
#12878=CARTESIAN_POINT('Ctrl Pts',(-0.23094010767585,0.0472735643746089,
-0.4));
#12879=CARTESIAN_POINT('Ctrl Pts',(-0.346410161513775,-0.0193931022920578,
-0.2));
#12880=CARTESIAN_POINT('Ctrl Pts',(-0.461880215351701,0.0472735643746089,
-5.6564012731995E-17));
#12881=CARTESIAN_POINT('',(0.23094010767585,0.0472735643746089,-0.4));
#12882=CARTESIAN_POINT('Ctrl Pts',(0.23094010767585,0.0472735643746089,
-0.4));
#12883=CARTESIAN_POINT('Ctrl Pts',(0.,-0.0193931022920578,-0.4));
#12884=CARTESIAN_POINT('Ctrl Pts',(-0.23094010767585,0.0472735643746089,
-0.4));
#12885=CARTESIAN_POINT('',(0.461880215351701,0.0472735643746089,0.));
#12886=CARTESIAN_POINT('Ctrl Pts',(0.461880215351701,0.0472735643746089,
0.));
#12887=CARTESIAN_POINT('Ctrl Pts',(0.346410161513776,-0.019393102292058,
-0.2));
#12888=CARTESIAN_POINT('Ctrl Pts',(0.23094010767585,0.0472735643746089,
-0.4));
#12889=CARTESIAN_POINT('Ctrl Pts',(0.23094010767585,0.0472735643746089,
0.4));
#12890=CARTESIAN_POINT('Ctrl Pts',(0.346410161513776,-0.0193931022920577,
0.2));
#12891=CARTESIAN_POINT('Ctrl Pts',(0.461880215351701,0.0472735643746089,
0.));
#12892=CARTESIAN_POINT('Origin',(0.,0.417495704353214,0.));
#12893=CARTESIAN_POINT('',(-0.38,0.47,-4.65365783675994E-17));
#12894=CARTESIAN_POINT('Origin',(0.,0.47,0.));
#12895=CARTESIAN_POINT('',(-0.461880215351701,0.422726435625391,-5.6564012731995E-17));
#12896=CARTESIAN_POINT('',(-0.47094010767585,0.417495704353214,-5.7673529545534E-17));
#12897=CARTESIAN_POINT('',(-0.230940107675851,0.422726435625391,0.4));
#12898=CARTESIAN_POINT('Ctrl Pts',(-0.230940107675851,0.422726435625391,
0.4));
#12899=CARTESIAN_POINT('Ctrl Pts',(-0.346410161513776,0.489393102292058,
0.2));
#12900=CARTESIAN_POINT('Ctrl Pts',(-0.461880215351701,0.422726435625391,
-5.6564012731995E-17));
#12901=CARTESIAN_POINT('',(0.23094010767585,0.422726435625391,0.4));
#12902=CARTESIAN_POINT('Ctrl Pts',(0.23094010767585,0.422726435625391,0.4));
#12903=CARTESIAN_POINT('Ctrl Pts',(8.32667268468867E-17,0.489393102292058,
0.4));
#12904=CARTESIAN_POINT('Ctrl Pts',(-0.230940107675851,0.422726435625391,
0.4));
#12905=CARTESIAN_POINT('',(0.461880215351701,0.422726435625391,0.));
#12906=CARTESIAN_POINT('Ctrl Pts',(0.461880215351701,0.422726435625391,
0.));
#12907=CARTESIAN_POINT('Ctrl Pts',(0.346410161513776,0.489393102292058,
0.2));
#12908=CARTESIAN_POINT('Ctrl Pts',(0.23094010767585,0.422726435625391,0.4));
#12909=CARTESIAN_POINT('',(0.23094010767585,0.422726435625391,-0.4));
#12910=CARTESIAN_POINT('Ctrl Pts',(0.23094010767585,0.422726435625391,-0.4));
#12911=CARTESIAN_POINT('Ctrl Pts',(0.346410161513775,0.489393102292058,
-0.2));
#12912=CARTESIAN_POINT('Ctrl Pts',(0.461880215351701,0.422726435625391,
0.));
#12913=CARTESIAN_POINT('',(-0.23094010767585,0.422726435625391,-0.4));
#12914=CARTESIAN_POINT('Ctrl Pts',(-0.23094010767585,0.422726435625391,
-0.4));
#12915=CARTESIAN_POINT('Ctrl Pts',(-5.55111512312578E-17,0.489393102292058,
-0.4));
#12916=CARTESIAN_POINT('Ctrl Pts',(0.23094010767585,0.422726435625391,-0.4));
#12917=CARTESIAN_POINT('Ctrl Pts',(-0.461880215351701,0.422726435625391,
-5.6564012731995E-17));
#12918=CARTESIAN_POINT('Ctrl Pts',(-0.346410161513776,0.489393102292058,
-0.2));
#12919=CARTESIAN_POINT('Ctrl Pts',(-0.23094010767585,0.422726435625391,
-0.4));
#12920=CARTESIAN_POINT('Origin',(0.23094010767585,0.,-0.4));
#12921=CARTESIAN_POINT('',(-0.23094010767585,0.,-0.4));
#12922=CARTESIAN_POINT('',(0.23094010767585,0.,-0.4));
#12923=CARTESIAN_POINT('Origin',(-0.23094010767585,0.,-0.4));
#12924=CARTESIAN_POINT('',(-0.461880215351701,0.,-5.6564012731995E-17));
#12925=CARTESIAN_POINT('Origin',(-0.461880215351701,0.,-5.6564012731995E-17));
#12926=CARTESIAN_POINT('',(-0.230940107675851,0.,0.4));
#12927=CARTESIAN_POINT('Origin',(0.,0.,0.));
#12928=CARTESIAN_POINT('',(-0.2117,0.47,2.59257727379495E-17));
#12929=CARTESIAN_POINT('Origin',(0.,0.47,0.));
#12930=CARTESIAN_POINT('',(-0.2117,0.,2.59257727379495E-17));
#12931=CARTESIAN_POINT('',(-0.2117,0.,2.59257727379495E-17));
#12932=CARTESIAN_POINT('Origin',(0.,0.,0.));
#12933=CARTESIAN_POINT('Origin',(-0.230940107675851,0.,0.4));
#12934=CARTESIAN_POINT('',(0.23094010767585,0.,0.4));
#12935=CARTESIAN_POINT('Origin',(0.461880215351701,0.,0.));
#12936=CARTESIAN_POINT('',(0.461880215351701,0.,0.));
#12937=CARTESIAN_POINT('Origin',(0.23094010767585,0.,0.4));
#12938=CARTESIAN_POINT('Origin',(0.,0.47,0.));
#12939=CARTESIAN_POINT('Origin',(0.,0.,0.));
#14318=UNCERTAINTY_MEASURE_WITH_UNIT(LENGTH_MEASURE(0.001),#14393,
'DISTANCE_ACCURACY_VALUE',
'Maximum model space distance between geometric entities at asserted c
onnectivities');
#14344=UNCERTAINTY_MEASURE_WITH_UNIT(LENGTH_MEASURE(0.001),#14393,
'DISTANCE_ACCURACY_VALUE',
'Maximum model space distance between geometric entities at asserted c
onnectivities');
#14366=(
GEOMETRIC_REPRESENTATION_CONTEXT(3)
GLOBAL_UNCERTAINTY_ASSIGNED_CONTEXT((#14318))
GLOBAL_UNIT_ASSIGNED_CONTEXT((#14393,#14395,#14396))
REPRESENTATION_CONTEXT('','3D')
);
#14392=(
GEOMETRIC_REPRESENTATION_CONTEXT(3)
GLOBAL_UNCERTAINTY_ASSIGNED_CONTEXT((#14344))
GLOBAL_UNIT_ASSIGNED_CONTEXT((#14393,#14395,#14396))
REPRESENTATION_CONTEXT('','3D')
);
#14393=(
LENGTH_UNIT()
NAMED_UNIT(*)
SI_UNIT(.CENTI.,.METRE.)
);
#14395=(
NAMED_UNIT(*)
PLANE_ANGLE_UNIT()
SI_UNIT($,.RADIAN.)
);
#14396=(
NAMED_UNIT(*)
SI_UNIT($,.STERADIAN.)
SOLID_ANGLE_UNIT()
);
#14418=SHAPE_DEFINITION_REPRESENTATION(#14467,#14604);
#14467=PRODUCT_DEFINITION_SHAPE('',$,#14652);
#14604=SHAPE_REPRESENTATION('',(#8809),#14366);
#14630=PRODUCT_DEFINITION_CONTEXT('part definition',#14773,'design');
#14652=PRODUCT_DEFINITION('Hex Nut - M5','Hex Nut - M5',#14699,#14630);
#14699=PRODUCT_DEFINITION_FORMATION('',$,#14796);
#14773=APPLICATION_CONTEXT(
'Core Data for Automotive Mechanical Design Process');
#14774=PRODUCT_CONTEXT('part definition',#14773,'mechanical');
#14796=PRODUCT('Hex Nut - M5','Hex Nut - M5','Hex Nut - M5',(#14774));
#14892=COLOUR_RGB('Black',0.12,0.14,0.17);
#14893=FILL_AREA_STYLE_COLOUR('',#14892);
#14894=FILL_AREA_STYLE('',(#14893));
#14895=SURFACE_STYLE_FILL_AREA(#14894);
#14896=SURFACE_SIDE_STYLE('',(#14895));
#14897=SURFACE_STYLE_USAGE(.BOTH.,#14896);
#14898=PRESENTATION_STYLE_ASSIGNMENT((#14897));
ENDSEC;
END-ISO-10303-21;
